ISO-10303-21;
HEADER;
/* Generated by software containing ST-Developer
 * from STEP Tools, Inc. (www.steptools.com) 
 */

FILE_DESCRIPTION(
/* description */ (''),
/* implementation_level */ '2;1');

FILE_NAME(
/* name */ 'Binding Head Screw JIS B 1111 - M2x6 Steel 4.6 Plain v1.step',
/* time_stamp */ '2026-10-07T02:13:48+06:00',
/* author */ (''),
/* organization */ (''),
/* preprocessor_version */ 'ST-DEVELOPER v20.2',
/* originating_system */ 'Autodesk Translation Framework v15.15.0.0',
/* authorisation */ '');

FILE_SCHEMA (('AUTOMOTIVE_DESIGN { 1 0 10303 214 3 1 1 }'));
ENDSEC;

DATA;
#10=MECHANICAL_DESIGN_GEOMETRIC_PRESENTATION_REPRESENTATION('',(#122),#17042);
#62=CONICAL_SURFACE('',#9046,0.919615242270664,0.261799387799148);
#63=CONICAL_SURFACE('',#9055,2.11281731799709,0.0872664626099693);
#98=SHAPE_REPRESENTATION_RELATIONSHIP('SRR','None',#17094,#110);
#110=ADVANCED_BREP_SHAPE_REPRESENTATION('',(#134),#17038);
#122=STYLED_ITEM('',(#17154),#134);
#134=MANIFOLD_SOLID_BREP('Body1',#8123);
#174=FACE_BOUND('',#1385,.T.);
#210=SPHERICAL_SURFACE('',#9051,6.32965591734106);
#233=TOROIDAL_SURFACE('',#9038,0.939230484541328,0.1);
#252=ELLIPSE('',#8997,0.992,0.496);
#253=ELLIPSE('',#8999,0.992,0.496);
#254=ELLIPSE('',#9004,0.992,0.496);
#255=ELLIPSE('',#9009,0.992,0.496);
#256=ELLIPSE('',#9014,0.992,0.496);
#257=ELLIPSE('',#9018,0.992,0.496);
#258=ELLIPSE('',#9020,0.992,0.496);
#259=ELLIPSE('',#9025,0.992,0.496);
#416=PLANE('',#9000);
#417=PLANE('',#9002);
#418=PLANE('',#9005);
#419=PLANE('',#9010);
#420=PLANE('',#9012);
#421=PLANE('',#9015);
#422=PLANE('',#9021);
#423=PLANE('',#9026);
#424=PLANE('',#9028);
#425=PLANE('',#9030);
#426=PLANE('',#9033);
#427=PLANE('',#9035);
#428=PLANE('',#9037);
#429=PLANE('',#9042);
#430=PLANE('',#9050);
#853=FACE_OUTER_BOUND('',#1366,.T.);
#854=FACE_OUTER_BOUND('',#1367,.T.);
#855=FACE_OUTER_BOUND('',#1368,.T.);
#856=FACE_OUTER_BOUND('',#1369,.T.);
#857=FACE_OUTER_BOUND('',#1370,.T.);
#858=FACE_OUTER_BOUND('',#1371,.T.);
#859=FACE_OUTER_BOUND('',#1372,.T.);
#860=FACE_OUTER_BOUND('',#1373,.T.);
#861=FACE_OUTER_BOUND('',#1374,.T.);
#862=FACE_OUTER_BOUND('',#1375,.T.);
#863=FACE_OUTER_BOUND('',#1376,.T.);
#864=FACE_OUTER_BOUND('',#1377,.T.);
#865=FACE_OUTER_BOUND('',#1378,.T.);
#866=FACE_OUTER_BOUND('',#1379,.T.);
#867=FACE_OUTER_BOUND('',#1380,.T.);
#868=FACE_OUTER_BOUND('',#1381,.T.);
#869=FACE_OUTER_BOUND('',#1382,.T.);
#870=FACE_OUTER_BOUND('',#1383,.T.);
#871=FACE_OUTER_BOUND('',#1384,.T.);
#872=FACE_OUTER_BOUND('',#1386,.T.);
#873=FACE_OUTER_BOUND('',#1387,.T.);
#874=FACE_OUTER_BOUND('',#1388,.T.);
#875=FACE_OUTER_BOUND('',#1389,.T.);
#876=FACE_OUTER_BOUND('',#1390,.T.);
#877=FACE_OUTER_BOUND('',#1391,.T.);
#1366=EDGE_LOOP('',(#6939,#6940,#6941,#6942,#6943,#6944));
#1367=EDGE_LOOP('',(#6945,#6946,#6947));
#1368=EDGE_LOOP('',(#6948,#6949,#6950,#6951,#6952,#6953));
#1369=EDGE_LOOP('',(#6954,#6955,#6956));
#1370=EDGE_LOOP('',(#6957,#6958,#6959,#6960,#6961,#6962));
#1371=EDGE_LOOP('',(#6963,#6964,#6965));
#1372=EDGE_LOOP('',(#6966,#6967,#6968,#6969,#6970,#6971));
#1373=EDGE_LOOP('',(#6972,#6973,#6974));
#1374=EDGE_LOOP('',(#6975,#6976,#6977,#6978,#6979,#6980));
#1375=EDGE_LOOP('',(#6981,#6982,#6983));
#1376=EDGE_LOOP('',(#6984,#6985,#6986,#6987,#6988,#6989));
#1377=EDGE_LOOP('',(#6990,#6991,#6992));
#1378=EDGE_LOOP('',(#6993,#6994,#6995));
#1379=EDGE_LOOP('',(#6996,#6997,#6998,#6999,#7000,#7001,#7002));
#1380=EDGE_LOOP('',(#7003,#7004,#7005));
#1381=EDGE_LOOP('',(#7006,#7007,#7008,#7009,#7010,#7011));
#1382=EDGE_LOOP('',(#7012,#7013,#7014,#7015,#7016,#7017,#7018,#7019));
#1383=EDGE_LOOP('',(#7020,#7021,#7022,#7023));
#1384=EDGE_LOOP('',(#7024));
#1385=EDGE_LOOP('',(#7025));
#1386=EDGE_LOOP('',(#7026,#7027,#7028,#7029));
#1387=EDGE_LOOP('',(#7030,#7031,#7032,#7033));
#1388=EDGE_LOOP('',(#7034,#7035,#7036,#7037));
#1389=EDGE_LOOP('',(#7038));
#1390=EDGE_LOOP('',(#7039,#7040,#7041,#7042,#7043,#7044,#7045,#7046,#7047,
#7048,#7049,#7050,#7051,#7052,#7053,#7054,#7055,#7056,#7057,#7058,#7059));
#1391=EDGE_LOOP('',(#7060,#7061,#7062,#7063,#7064));
#1842=CIRCLE('',#8998,0.496);
#1843=CIRCLE('',#9001,6.32479565138939);
#1844=CIRCLE('',#9003,5.93049029404341);
#1845=CIRCLE('',#9006,6.32479565138933);
#1846=CIRCLE('',#9008,0.496);
#1847=CIRCLE('',#9011,6.32479565138941);
#1848=CIRCLE('',#9013,5.93049029404341);
#1849=CIRCLE('',#9016,6.32479565138941);
#1850=CIRCLE('',#9019,0.496);
#1851=CIRCLE('',#9022,6.32479565138943);
#1852=CIRCLE('',#9024,0.496);
#1853=CIRCLE('',#9027,6.32479565138944);
#1854=CIRCLE('',#9029,6.32479565138933);
#1855=CIRCLE('',#9031,5.93049029404347);
#1856=CIRCLE('',#9032,5.93049029404347);
#1857=CIRCLE('',#9034,6.32479565138944);
#1858=CIRCLE('',#9036,5.93049029404341);
#1859=CIRCLE('',#9039,0.939230484541328);
#1860=CIRCLE('',#9040,0.1);
#1861=CIRCLE('',#9041,0.839230484541328);
#1862=CIRCLE('',#9043,2.15);
#1863=CIRCLE('',#9045,0.839230484541328);
#1864=CIRCLE('',#9047,0.96675);
#1865=CIRCLE('',#9049,0.96675);
#1866=CIRCLE('',#9052,6.32965591734106);
#1867=CIRCLE('',#9053,2.07563463599418);
#1868=CIRCLE('',#9054,2.07563463599418);
#2006=B_SPLINE_CURVE_WITH_KNOTS('',3,(#16263,#16264,#16265,#16266,#16267,
#16268,#16269,#16270,#16271,#16272,#16273,#16274,#16275,#16276,#16277),
 .UNSPECIFIED.,.F.,.F.,(4,2,2,3,2,2,4),(-0.0374758352523592,-0.0373394553501654,
-0.0186697276750827,0.,0.0186697276750831,0.0373394553501661,0.0374758352523223),
 .UNSPECIFIED.);
#2007=B_SPLINE_CURVE_WITH_KNOTS('',3,(#16305,#16306,#16307,#16308,#16309,
#16310,#16311,#16312,#16313,#16314,#16315,#16316,#16317,#16318,#16319),
 .UNSPECIFIED.,.F.,.F.,(4,2,2,3,2,2,4),(-0.0374758352523656,-0.0373394553501654,
-0.0186697276750827,0.,0.0186697276750831,0.0373394553501662,0.0374758352523289),
 .UNSPECIFIED.);
#2008=B_SPLINE_CURVE_WITH_KNOTS('',3,(#16344,#16345,#16346,#16347,#16348,
#16349,#16350,#16351,#16352,#16353,#16354,#16355,#16356,#16357,#16358),
 .UNSPECIFIED.,.F.,.F.,(4,2,2,3,2,2,4),(-0.0374758352524519,-0.0373394553501659,
-0.0186697276750829,0.,0.0186697276750829,0.0373394553501658,0.0374758352524142),
 .UNSPECIFIED.);
#2009=B_SPLINE_CURVE_WITH_KNOTS('',3,(#16374,#16375,#16376,#16377,#16378,
#16379,#16380,#16381,#16382,#16383,#16384,#16385,#16386,#16387,#16388),
 .UNSPECIFIED.,.F.,.F.,(4,2,2,3,2,2,4),(-0.0374758352524171,-0.0373394553501658,
-0.0186697276750829,0.,0.018669727675083,0.037339455350166,0.0374758352523797),
 .UNSPECIFIED.);
#2504=LINE('',#16279,#3082);
#2505=LINE('',#16286,#3083);
#2506=LINE('',#16290,#3084);
#2507=LINE('',#16295,#3085);
#2508=LINE('',#16298,#3086);
#2509=LINE('',#16302,#3087);
#2510=LINE('',#16324,#3088);
#2511=LINE('',#16328,#3089);
#2512=LINE('',#16333,#3090);
#2513=LINE('',#16336,#3091);
#2514=LINE('',#16340,#3092);
#2515=LINE('',#16360,#3093);
#2516=LINE('',#16367,#3094);
#2517=LINE('',#16371,#3095);
#2518=LINE('',#16393,#3096);
#2519=LINE('',#16397,#3097);
#2520=LINE('',#16401,#3098);
#2521=LINE('',#16405,#3099);
#2522=LINE('',#16410,#3100);
#2523=LINE('',#16413,#3101);
#2524=LINE('',#16427,#3102);
#2525=LINE('',#16431,#3103);
#2526=LINE('',#16435,#3104);
#2527=LINE('',#16444,#3105);
#3082=VECTOR('',#11207,10.);
#3083=VECTOR('',#11214,10.);
#3084=VECTOR('',#11219,10.);
#3085=VECTOR('',#11224,10.);
#3086=VECTOR('',#11227,10.);
#3087=VECTOR('',#11232,10.);
#3088=VECTOR('',#11239,10.);
#3089=VECTOR('',#11244,10.);
#3090=VECTOR('',#11249,10.);
#3091=VECTOR('',#11252,10.);
#3092=VECTOR('',#11257,10.);
#3093=VECTOR('',#11260,10.);
#3094=VECTOR('',#11267,10.);
#3095=VECTOR('',#11272,10.);
#3096=VECTOR('',#11279,10.);
#3097=VECTOR('',#11284,10.);
#3098=VECTOR('',#11289,10.);
#3099=VECTOR('',#11294,10.);
#3100=VECTOR('',#11301,10.);
#3101=VECTOR('',#11306,10.);
#3102=VECTOR('',#11325,0.839230484541328);
#3103=VECTOR('',#11330,0.919615242270664);
#3104=VECTOR('',#11335,1.);
#3105=VECTOR('',#11348,2.11281731799709);
#3748=VERTEX_POINT('',#16261);
#3749=VERTEX_POINT('',#16262);
#3750=VERTEX_POINT('',#16278);
#3751=VERTEX_POINT('',#16280);
#3752=VERTEX_POINT('',#16282);
#3753=VERTEX_POINT('',#16284);
#3754=VERTEX_POINT('',#16288);
#3755=VERTEX_POINT('',#16292);
#3756=VERTEX_POINT('',#16294);
#3757=VERTEX_POINT('',#16296);
#3758=VERTEX_POINT('',#16300);
#3759=VERTEX_POINT('',#16304);
#3760=VERTEX_POINT('',#16320);
#3761=VERTEX_POINT('',#16322);
#3762=VERTEX_POINT('',#16326);
#3763=VERTEX_POINT('',#16330);
#3764=VERTEX_POINT('',#16332);
#3765=VERTEX_POINT('',#16334);
#3766=VERTEX_POINT('',#16338);
#3767=VERTEX_POINT('',#16342);
#3768=VERTEX_POINT('',#16343);
#3769=VERTEX_POINT('',#16359);
#3770=VERTEX_POINT('',#16361);
#3771=VERTEX_POINT('',#16363);
#3772=VERTEX_POINT('',#16365);
#3773=VERTEX_POINT('',#16369);
#3774=VERTEX_POINT('',#16373);
#3775=VERTEX_POINT('',#16389);
#3776=VERTEX_POINT('',#16391);
#3777=VERTEX_POINT('',#16395);
#3778=VERTEX_POINT('',#16399);
#3779=VERTEX_POINT('',#16403);
#3780=VERTEX_POINT('',#16408);
#3781=VERTEX_POINT('',#16416);
#3782=VERTEX_POINT('',#16418);
#3783=VERTEX_POINT('',#16422);
#3784=VERTEX_POINT('',#16425);
#3785=VERTEX_POINT('',#16429);
#3786=VERTEX_POINT('',#16433);
#3787=VERTEX_POINT('',#16438);
#3788=VERTEX_POINT('',#16440);
#4837=EDGE_CURVE('',#3748,#3749,#2006,.T.);
#4838=EDGE_CURVE('',#3750,#3748,#2504,.T.);
#4839=EDGE_CURVE('',#3750,#3751,#252,.F.);
#4840=EDGE_CURVE('',#3751,#3752,#1842,.F.);
#4841=EDGE_CURVE('',#3753,#3752,#253,.T.);
#4842=EDGE_CURVE('',#3749,#3753,#2505,.T.);
#4843=EDGE_CURVE('',#3749,#3754,#1843,.T.);
#4844=EDGE_CURVE('',#3754,#3753,#2506,.F.);
#4845=EDGE_CURVE('',#3754,#3755,#1844,.T.);
#4846=EDGE_CURVE('',#3752,#3756,#2507,.F.);
#4847=EDGE_CURVE('',#3757,#3756,#254,.F.);
#4848=EDGE_CURVE('',#3755,#3757,#2508,.T.);
#4849=EDGE_CURVE('',#3755,#3758,#1845,.T.);
#4850=EDGE_CURVE('',#3757,#3758,#2509,.T.);
#4851=EDGE_CURVE('',#3758,#3759,#2007,.T.);
#4852=EDGE_CURVE('',#3756,#3760,#1846,.F.);
#4853=EDGE_CURVE('',#3761,#3760,#255,.T.);
#4854=EDGE_CURVE('',#3759,#3761,#2510,.T.);
#4855=EDGE_CURVE('',#3759,#3762,#1847,.T.);
#4856=EDGE_CURVE('',#3762,#3761,#2511,.F.);
#4857=EDGE_CURVE('',#3762,#3763,#1848,.T.);
#4858=EDGE_CURVE('',#3760,#3764,#2512,.F.);
#4859=EDGE_CURVE('',#3765,#3764,#256,.F.);
#4860=EDGE_CURVE('',#3763,#3765,#2513,.T.);
#4861=EDGE_CURVE('',#3763,#3766,#1849,.T.);
#4862=EDGE_CURVE('',#3765,#3766,#2514,.T.);
#4863=EDGE_CURVE('',#3767,#3768,#2008,.T.);
#4864=EDGE_CURVE('',#3769,#3767,#2515,.T.);
#4865=EDGE_CURVE('',#3769,#3770,#257,.F.);
#4866=EDGE_CURVE('',#3770,#3771,#1850,.F.);
#4867=EDGE_CURVE('',#3772,#3771,#258,.T.);
#4868=EDGE_CURVE('',#3768,#3772,#2516,.T.);
#4869=EDGE_CURVE('',#3768,#3773,#1851,.T.);
#4870=EDGE_CURVE('',#3773,#3772,#2517,.F.);
#4871=EDGE_CURVE('',#3766,#3774,#2009,.T.);
#4872=EDGE_CURVE('',#3764,#3775,#1852,.F.);
#4873=EDGE_CURVE('',#3776,#3775,#259,.T.);
#4874=EDGE_CURVE('',#3774,#3776,#2518,.T.);
#4875=EDGE_CURVE('',#3774,#3777,#1853,.T.);
#4876=EDGE_CURVE('',#3777,#3776,#2519,.F.);
#4877=EDGE_CURVE('',#3778,#3748,#1854,.T.);
#4878=EDGE_CURVE('',#3778,#3750,#2520,.T.);
#4879=EDGE_CURVE('',#3773,#3779,#1855,.T.);
#4880=EDGE_CURVE('',#3771,#3751,#2521,.F.);
#4881=EDGE_CURVE('',#3779,#3778,#1856,.T.);
#4882=EDGE_CURVE('',#3780,#3767,#1857,.T.);
#4883=EDGE_CURVE('',#3780,#3769,#2522,.T.);
#4884=EDGE_CURVE('',#3777,#3780,#1858,.T.);
#4885=EDGE_CURVE('',#3775,#3770,#2523,.F.);
#4886=EDGE_CURVE('',#3781,#3781,#1859,.T.);
#4887=EDGE_CURVE('',#3781,#3782,#1860,.T.);
#4888=EDGE_CURVE('',#3782,#3782,#1861,.T.);
#4889=EDGE_CURVE('',#3783,#3783,#1862,.T.);
#4890=EDGE_CURVE('',#3784,#3784,#1863,.T.);
#4891=EDGE_CURVE('',#3784,#3782,#2524,.T.);
#4892=EDGE_CURVE('',#3785,#3785,#1864,.T.);
#4893=EDGE_CURVE('',#3785,#3784,#2525,.T.);
#4894=EDGE_CURVE('',#3786,#3786,#1865,.F.);
#4895=EDGE_CURVE('',#3786,#3785,#2526,.T.);
#4896=EDGE_CURVE('',#3779,#3787,#1866,.T.);
#4897=EDGE_CURVE('',#3788,#3787,#1867,.T.);
#4898=EDGE_CURVE('',#3787,#3788,#1868,.T.);
#4899=EDGE_CURVE('',#3783,#3788,#2527,.T.);
#6939=ORIENTED_EDGE('',*,*,#4837,.F.);
#6940=ORIENTED_EDGE('',*,*,#4838,.F.);
#6941=ORIENTED_EDGE('',*,*,#4839,.T.);
#6942=ORIENTED_EDGE('',*,*,#4840,.T.);
#6943=ORIENTED_EDGE('',*,*,#4841,.F.);
#6944=ORIENTED_EDGE('',*,*,#4842,.F.);
#6945=ORIENTED_EDGE('',*,*,#4843,.F.);
#6946=ORIENTED_EDGE('',*,*,#4842,.T.);
#6947=ORIENTED_EDGE('',*,*,#4844,.F.);
#6948=ORIENTED_EDGE('',*,*,#4845,.F.);
#6949=ORIENTED_EDGE('',*,*,#4844,.T.);
#6950=ORIENTED_EDGE('',*,*,#4841,.T.);
#6951=ORIENTED_EDGE('',*,*,#4846,.T.);
#6952=ORIENTED_EDGE('',*,*,#4847,.F.);
#6953=ORIENTED_EDGE('',*,*,#4848,.F.);
#6954=ORIENTED_EDGE('',*,*,#4849,.F.);
#6955=ORIENTED_EDGE('',*,*,#4848,.T.);
#6956=ORIENTED_EDGE('',*,*,#4850,.T.);
#6957=ORIENTED_EDGE('',*,*,#4851,.F.);
#6958=ORIENTED_EDGE('',*,*,#4850,.F.);
#6959=ORIENTED_EDGE('',*,*,#4847,.T.);
#6960=ORIENTED_EDGE('',*,*,#4852,.T.);
#6961=ORIENTED_EDGE('',*,*,#4853,.F.);
#6962=ORIENTED_EDGE('',*,*,#4854,.F.);
#6963=ORIENTED_EDGE('',*,*,#4855,.F.);
#6964=ORIENTED_EDGE('',*,*,#4854,.T.);
#6965=ORIENTED_EDGE('',*,*,#4856,.F.);
#6966=ORIENTED_EDGE('',*,*,#4857,.F.);
#6967=ORIENTED_EDGE('',*,*,#4856,.T.);
#6968=ORIENTED_EDGE('',*,*,#4853,.T.);
#6969=ORIENTED_EDGE('',*,*,#4858,.T.);
#6970=ORIENTED_EDGE('',*,*,#4859,.F.);
#6971=ORIENTED_EDGE('',*,*,#4860,.F.);
#6972=ORIENTED_EDGE('',*,*,#4861,.F.);
#6973=ORIENTED_EDGE('',*,*,#4860,.T.);
#6974=ORIENTED_EDGE('',*,*,#4862,.T.);
#6975=ORIENTED_EDGE('',*,*,#4863,.F.);
#6976=ORIENTED_EDGE('',*,*,#4864,.F.);
#6977=ORIENTED_EDGE('',*,*,#4865,.T.);
#6978=ORIENTED_EDGE('',*,*,#4866,.T.);
#6979=ORIENTED_EDGE('',*,*,#4867,.F.);
#6980=ORIENTED_EDGE('',*,*,#4868,.F.);
#6981=ORIENTED_EDGE('',*,*,#4869,.F.);
#6982=ORIENTED_EDGE('',*,*,#4868,.T.);
#6983=ORIENTED_EDGE('',*,*,#4870,.F.);
#6984=ORIENTED_EDGE('',*,*,#4871,.F.);
#6985=ORIENTED_EDGE('',*,*,#4862,.F.);
#6986=ORIENTED_EDGE('',*,*,#4859,.T.);
#6987=ORIENTED_EDGE('',*,*,#4872,.T.);
#6988=ORIENTED_EDGE('',*,*,#4873,.F.);
#6989=ORIENTED_EDGE('',*,*,#4874,.F.);
#6990=ORIENTED_EDGE('',*,*,#4875,.F.);
#6991=ORIENTED_EDGE('',*,*,#4874,.T.);
#6992=ORIENTED_EDGE('',*,*,#4876,.F.);
#6993=ORIENTED_EDGE('',*,*,#4877,.F.);
#6994=ORIENTED_EDGE('',*,*,#4878,.T.);
#6995=ORIENTED_EDGE('',*,*,#4838,.T.);
#6996=ORIENTED_EDGE('',*,*,#4879,.F.);
#6997=ORIENTED_EDGE('',*,*,#4870,.T.);
#6998=ORIENTED_EDGE('',*,*,#4867,.T.);
#6999=ORIENTED_EDGE('',*,*,#4880,.T.);
#7000=ORIENTED_EDGE('',*,*,#4839,.F.);
#7001=ORIENTED_EDGE('',*,*,#4878,.F.);
#7002=ORIENTED_EDGE('',*,*,#4881,.F.);
#7003=ORIENTED_EDGE('',*,*,#4882,.F.);
#7004=ORIENTED_EDGE('',*,*,#4883,.T.);
#7005=ORIENTED_EDGE('',*,*,#4864,.T.);
#7006=ORIENTED_EDGE('',*,*,#4884,.F.);
#7007=ORIENTED_EDGE('',*,*,#4876,.T.);
#7008=ORIENTED_EDGE('',*,*,#4873,.T.);
#7009=ORIENTED_EDGE('',*,*,#4885,.T.);
#7010=ORIENTED_EDGE('',*,*,#4865,.F.);
#7011=ORIENTED_EDGE('',*,*,#4883,.F.);
#7012=ORIENTED_EDGE('',*,*,#4846,.F.);
#7013=ORIENTED_EDGE('',*,*,#4840,.F.);
#7014=ORIENTED_EDGE('',*,*,#4880,.F.);
#7015=ORIENTED_EDGE('',*,*,#4866,.F.);
#7016=ORIENTED_EDGE('',*,*,#4885,.F.);
#7017=ORIENTED_EDGE('',*,*,#4872,.F.);
#7018=ORIENTED_EDGE('',*,*,#4858,.F.);
#7019=ORIENTED_EDGE('',*,*,#4852,.F.);
#7020=ORIENTED_EDGE('',*,*,#4886,.T.);
#7021=ORIENTED_EDGE('',*,*,#4887,.T.);
#7022=ORIENTED_EDGE('',*,*,#4888,.T.);
#7023=ORIENTED_EDGE('',*,*,#4887,.F.);
#7024=ORIENTED_EDGE('',*,*,#4889,.T.);
#7025=ORIENTED_EDGE('',*,*,#4886,.F.);
#7026=ORIENTED_EDGE('',*,*,#4890,.F.);
#7027=ORIENTED_EDGE('',*,*,#4891,.T.);
#7028=ORIENTED_EDGE('',*,*,#4888,.F.);
#7029=ORIENTED_EDGE('',*,*,#4891,.F.);
#7030=ORIENTED_EDGE('',*,*,#4892,.F.);
#7031=ORIENTED_EDGE('',*,*,#4893,.T.);
#7032=ORIENTED_EDGE('',*,*,#4890,.T.);
#7033=ORIENTED_EDGE('',*,*,#4893,.F.);
#7034=ORIENTED_EDGE('',*,*,#4894,.F.);
#7035=ORIENTED_EDGE('',*,*,#4895,.T.);
#7036=ORIENTED_EDGE('',*,*,#4892,.T.);
#7037=ORIENTED_EDGE('',*,*,#4895,.F.);
#7038=ORIENTED_EDGE('',*,*,#4894,.T.);
#7039=ORIENTED_EDGE('',*,*,#4871,.T.);
#7040=ORIENTED_EDGE('',*,*,#4875,.T.);
#7041=ORIENTED_EDGE('',*,*,#4884,.T.);
#7042=ORIENTED_EDGE('',*,*,#4882,.T.);
#7043=ORIENTED_EDGE('',*,*,#4863,.T.);
#7044=ORIENTED_EDGE('',*,*,#4869,.T.);
#7045=ORIENTED_EDGE('',*,*,#4879,.T.);
#7046=ORIENTED_EDGE('',*,*,#4896,.T.);
#7047=ORIENTED_EDGE('',*,*,#4897,.F.);
#7048=ORIENTED_EDGE('',*,*,#4898,.F.);
#7049=ORIENTED_EDGE('',*,*,#4896,.F.);
#7050=ORIENTED_EDGE('',*,*,#4881,.T.);
#7051=ORIENTED_EDGE('',*,*,#4877,.T.);
#7052=ORIENTED_EDGE('',*,*,#4837,.T.);
#7053=ORIENTED_EDGE('',*,*,#4843,.T.);
#7054=ORIENTED_EDGE('',*,*,#4845,.T.);
#7055=ORIENTED_EDGE('',*,*,#4849,.T.);
#7056=ORIENTED_EDGE('',*,*,#4851,.T.);
#7057=ORIENTED_EDGE('',*,*,#4855,.T.);
#7058=ORIENTED_EDGE('',*,*,#4857,.T.);
#7059=ORIENTED_EDGE('',*,*,#4861,.T.);
#7060=ORIENTED_EDGE('',*,*,#4889,.F.);
#7061=ORIENTED_EDGE('',*,*,#4899,.T.);
#7062=ORIENTED_EDGE('',*,*,#4897,.T.);
#7063=ORIENTED_EDGE('',*,*,#4898,.T.);
#7064=ORIENTED_EDGE('',*,*,#4899,.F.);
#7614=CYLINDRICAL_SURFACE('',#8996,0.496);
#7615=CYLINDRICAL_SURFACE('',#9007,0.496);
#7616=CYLINDRICAL_SURFACE('',#9017,0.496);
#7617=CYLINDRICAL_SURFACE('',#9023,0.496);
#7618=CYLINDRICAL_SURFACE('',#9044,0.839230484541328);
#7619=CYLINDRICAL_SURFACE('',#9048,0.96675);
#8015=ADVANCED_FACE('',(#853),#7614,.T.);
#8016=ADVANCED_FACE('',(#854),#416,.F.);
#8017=ADVANCED_FACE('',(#855),#417,.F.);
#8018=ADVANCED_FACE('',(#856),#418,.F.);
#8019=ADVANCED_FACE('',(#857),#7615,.T.);
#8020=ADVANCED_FACE('',(#858),#419,.F.);
#8021=ADVANCED_FACE('',(#859),#420,.F.);
#8022=ADVANCED_FACE('',(#860),#421,.F.);
#8023=ADVANCED_FACE('',(#861),#7616,.T.);
#8024=ADVANCED_FACE('',(#862),#422,.F.);
#8025=ADVANCED_FACE('',(#863),#7617,.T.);
#8026=ADVANCED_FACE('',(#864),#423,.F.);
#8027=ADVANCED_FACE('',(#865),#424,.F.);
#8028=ADVANCED_FACE('',(#866),#425,.F.);
#8029=ADVANCED_FACE('',(#867),#426,.F.);
#8030=ADVANCED_FACE('',(#868),#427,.F.);
#8031=ADVANCED_FACE('',(#869),#428,.F.);
#8032=ADVANCED_FACE('',(#870),#233,.F.);
#8033=ADVANCED_FACE('',(#871,#174),#429,.T.);
#8034=ADVANCED_FACE('',(#872),#7618,.T.);
#8035=ADVANCED_FACE('',(#873),#62,.T.);
#8036=ADVANCED_FACE('',(#874),#7619,.T.);
#8037=ADVANCED_FACE('',(#875),#430,.T.);
#8038=ADVANCED_FACE('',(#876),#210,.T.);
#8039=ADVANCED_FACE('',(#877),#63,.T.);
#8123=CLOSED_SHELL('',(#8015,#8016,#8017,#8018,#8019,#8020,#8021,#8022,
#8023,#8024,#8025,#8026,#8027,#8028,#8029,#8030,#8031,#8032,#8033,#8034,
#8035,#8036,#8037,#8038,#8039));
#8995=AXIS2_PLACEMENT_3D('',#16259,#11203,#11204);
#8996=AXIS2_PLACEMENT_3D('',#16260,#11205,#11206);
#8997=AXIS2_PLACEMENT_3D('',#16281,#11208,#11209);
#8998=AXIS2_PLACEMENT_3D('',#16283,#11210,#11211);
#8999=AXIS2_PLACEMENT_3D('',#16285,#11212,#11213);
#9000=AXIS2_PLACEMENT_3D('',#16287,#11215,#11216);
#9001=AXIS2_PLACEMENT_3D('',#16289,#11217,#11218);
#9002=AXIS2_PLACEMENT_3D('',#16291,#11220,#11221);
#9003=AXIS2_PLACEMENT_3D('',#16293,#11222,#11223);
#9004=AXIS2_PLACEMENT_3D('',#16297,#11225,#11226);
#9005=AXIS2_PLACEMENT_3D('',#16299,#11228,#11229);
#9006=AXIS2_PLACEMENT_3D('',#16301,#11230,#11231);
#9007=AXIS2_PLACEMENT_3D('',#16303,#11233,#11234);
#9008=AXIS2_PLACEMENT_3D('',#16321,#11235,#11236);
#9009=AXIS2_PLACEMENT_3D('',#16323,#11237,#11238);
#9010=AXIS2_PLACEMENT_3D('',#16325,#11240,#11241);
#9011=AXIS2_PLACEMENT_3D('',#16327,#11242,#11243);
#9012=AXIS2_PLACEMENT_3D('',#16329,#11245,#11246);
#9013=AXIS2_PLACEMENT_3D('',#16331,#11247,#11248);
#9014=AXIS2_PLACEMENT_3D('',#16335,#11250,#11251);
#9015=AXIS2_PLACEMENT_3D('',#16337,#11253,#11254);
#9016=AXIS2_PLACEMENT_3D('',#16339,#11255,#11256);
#9017=AXIS2_PLACEMENT_3D('',#16341,#11258,#11259);
#9018=AXIS2_PLACEMENT_3D('',#16362,#11261,#11262);
#9019=AXIS2_PLACEMENT_3D('',#16364,#11263,#11264);
#9020=AXIS2_PLACEMENT_3D('',#16366,#11265,#11266);
#9021=AXIS2_PLACEMENT_3D('',#16368,#11268,#11269);
#9022=AXIS2_PLACEMENT_3D('',#16370,#11270,#11271);
#9023=AXIS2_PLACEMENT_3D('',#16372,#11273,#11274);
#9024=AXIS2_PLACEMENT_3D('',#16390,#11275,#11276);
#9025=AXIS2_PLACEMENT_3D('',#16392,#11277,#11278);
#9026=AXIS2_PLACEMENT_3D('',#16394,#11280,#11281);
#9027=AXIS2_PLACEMENT_3D('',#16396,#11282,#11283);
#9028=AXIS2_PLACEMENT_3D('',#16398,#11285,#11286);
#9029=AXIS2_PLACEMENT_3D('',#16400,#11287,#11288);
#9030=AXIS2_PLACEMENT_3D('',#16402,#11290,#11291);
#9031=AXIS2_PLACEMENT_3D('',#16404,#11292,#11293);
#9032=AXIS2_PLACEMENT_3D('',#16406,#11295,#11296);
#9033=AXIS2_PLACEMENT_3D('',#16407,#11297,#11298);
#9034=AXIS2_PLACEMENT_3D('',#16409,#11299,#11300);
#9035=AXIS2_PLACEMENT_3D('',#16411,#11302,#11303);
#9036=AXIS2_PLACEMENT_3D('',#16412,#11304,#11305);
#9037=AXIS2_PLACEMENT_3D('',#16414,#11307,#11308);
#9038=AXIS2_PLACEMENT_3D('',#16415,#11309,#11310);
#9039=AXIS2_PLACEMENT_3D('',#16417,#11311,#11312);
#9040=AXIS2_PLACEMENT_3D('',#16419,#11313,#11314);
#9041=AXIS2_PLACEMENT_3D('',#16420,#11315,#11316);
#9042=AXIS2_PLACEMENT_3D('',#16421,#11317,#11318);
#9043=AXIS2_PLACEMENT_3D('',#16423,#11319,#11320);
#9044=AXIS2_PLACEMENT_3D('',#16424,#11321,#11322);
#9045=AXIS2_PLACEMENT_3D('',#16426,#11323,#11324);
#9046=AXIS2_PLACEMENT_3D('',#16428,#11326,#11327);
#9047=AXIS2_PLACEMENT_3D('',#16430,#11328,#11329);
#9048=AXIS2_PLACEMENT_3D('',#16432,#11331,#11332);
#9049=AXIS2_PLACEMENT_3D('',#16434,#11333,#11334);
#9050=AXIS2_PLACEMENT_3D('',#16436,#11336,#11337);
#9051=AXIS2_PLACEMENT_3D('',#16437,#11338,#11339);
#9052=AXIS2_PLACEMENT_3D('',#16439,#11340,#11341);
#9053=AXIS2_PLACEMENT_3D('',#16441,#11342,#11343);
#9054=AXIS2_PLACEMENT_3D('',#16442,#11344,#11345);
#9055=AXIS2_PLACEMENT_3D('',#16443,#11346,#11347);
#11203=DIRECTION('axis',(0.,0.,1.));
#11204=DIRECTION('refdir',(1.,0.,0.));
#11205=DIRECTION('center_axis',(0.,0.,-1.));
#11206=DIRECTION('ref_axis',(0.707106781186864,-0.707106781186231,0.));
#11207=DIRECTION('',(0.,0.,1.));
#11208=DIRECTION('center_axis',(-0.866025403784439,2.42308806056559E-16,
-0.5));
#11209=DIRECTION('ref_axis',(0.5,-1.39897054514259E-16,-0.866025403784439));
#11210=DIRECTION('center_axis',(0.,0.,-1.));
#11211=DIRECTION('ref_axis',(0.707106781186864,-0.707106781186231,0.));
#11212=DIRECTION('center_axis',(-1.34432925600244E-12,0.866025403784439,
-0.5));
#11213=DIRECTION('ref_axis',(7.76183832708735E-13,-0.5,-0.866025403784439));
#11214=DIRECTION('',(0.,0.,-1.));
#11215=DIRECTION('center_axis',(-1.,-8.96558844583498E-13,0.));
#11216=DIRECTION('ref_axis',(-8.96558844583498E-13,1.,0.));
#11217=DIRECTION('center_axis',(-1.,-8.96558844583498E-13,0.));
#11218=DIRECTION('ref_axis',(0.,0.,-1.));
#11219=DIRECTION('',(-4.48279422291749E-13,0.5,0.866025403784439));
#11220=DIRECTION('center_axis',(-1.34432925600244E-12,0.866025403784439,
-0.5));
#11221=DIRECTION('ref_axis',(1.,1.55229771566499E-12,0.));
#11222=DIRECTION('center_axis',(-1.34432925600244E-12,0.866025403784439,
-0.5));
#11223=DIRECTION('ref_axis',(0.,-0.5,-0.866025403784439));
#11224=DIRECTION('',(-1.,-1.55229771566499E-12,0.));
#11225=DIRECTION('center_axis',(-1.34432925600244E-12,0.866025403784439,
-0.5));
#11226=DIRECTION('ref_axis',(7.76183832708735E-13,-0.5,-0.866025403784439));
#11227=DIRECTION('',(7.28095205575773E-14,-0.5,-0.866025403784439));
#11228=DIRECTION('center_axis',(1.,1.45619041115155E-13,0.));
#11229=DIRECTION('ref_axis',(1.45619041115155E-13,-1.,0.));
#11230=DIRECTION('center_axis',(1.,1.45619041115155E-13,0.));
#11231=DIRECTION('ref_axis',(0.,0.,1.));
#11232=DIRECTION('',(0.,0.,1.));
#11233=DIRECTION('center_axis',(0.,0.,-1.));
#11234=DIRECTION('ref_axis',(-0.707106781186035,-0.70710678118706,0.));
#11235=DIRECTION('center_axis',(0.,0.,-1.));
#11236=DIRECTION('ref_axis',(-0.707106781186035,-0.70710678118706,0.));
#11237=DIRECTION('center_axis',(0.866025403784439,1.82700839766916E-13,
-0.5));
#11238=DIRECTION('ref_axis',(-0.5,-1.0551735336738E-13,-0.866025403784439));
#11239=DIRECTION('',(0.,0.,-1.));
#11240=DIRECTION('center_axis',(-1.30466679482154E-12,1.,0.));
#11241=DIRECTION('ref_axis',(1.,1.30466679482154E-12,0.));
#11242=DIRECTION('center_axis',(-1.30466679482154E-12,1.,0.));
#11243=DIRECTION('ref_axis',(0.,0.,-1.));
#11244=DIRECTION('',(0.5,6.52333397410772E-13,0.866025403784439));
#11245=DIRECTION('center_axis',(0.866025403784439,1.82700839766916E-13,
-0.5));
#11246=DIRECTION('ref_axis',(2.10964758041199E-13,-1.,0.));
#11247=DIRECTION('center_axis',(0.866025403784439,1.82700839766916E-13,
-0.5));
#11248=DIRECTION('ref_axis',(0.5,0.,0.866025403784439));
#11249=DIRECTION('',(-2.10964758041199E-13,1.,0.));
#11250=DIRECTION('center_axis',(0.866025403784439,1.82700839766916E-13,
-0.5));
#11251=DIRECTION('ref_axis',(-0.5,-1.05482379103751E-13,-0.866025403784439));
#11252=DIRECTION('',(-0.5,6.4832235838889E-13,-0.866025403784439));
#11253=DIRECTION('center_axis',(-1.29664471677778E-12,-1.,0.));
#11254=DIRECTION('ref_axis',(-1.,1.29664471677778E-12,0.));
#11255=DIRECTION('center_axis',(-1.29664471677778E-12,-1.,0.));
#11256=DIRECTION('ref_axis',(0.,0.,1.));
#11257=DIRECTION('',(0.,0.,1.));
#11258=DIRECTION('center_axis',(0.,0.,-1.));
#11259=DIRECTION('ref_axis',(0.707106781186895,0.7071067811862,0.));
#11260=DIRECTION('',(0.,0.,1.));
#11261=DIRECTION('center_axis',(-1.35644469630397E-12,-0.866025403784439,
-0.5));
#11262=DIRECTION('ref_axis',(7.8314371117082E-13,0.5,-0.866025403784439));
#11263=DIRECTION('center_axis',(0.,0.,-1.));
#11264=DIRECTION('ref_axis',(0.707106781186895,0.7071067811862,0.));
#11265=DIRECTION('center_axis',(-0.866025403784439,2.42308806056559E-16,
-0.5));
#11266=DIRECTION('ref_axis',(0.5,-1.39897054514259E-16,-0.866025403784439));
#11267=DIRECTION('',(0.,0.,-1.));
#11268=DIRECTION('center_axis',(1.80920256647203E-12,-1.,0.));
#11269=DIRECTION('ref_axis',(-1.,-1.80920256647203E-12,0.));
#11270=DIRECTION('center_axis',(1.80920256647203E-12,-1.,0.));
#11271=DIRECTION('ref_axis',(0.,0.,1.));
#11272=DIRECTION('',(-0.5,-9.04601283236015E-13,0.866025403784439));
#11273=DIRECTION('center_axis',(0.,0.,-1.));
#11274=DIRECTION('ref_axis',(-0.707106781186768,0.707106781186327,0.));
#11275=DIRECTION('center_axis',(0.,0.,-1.));
#11276=DIRECTION('ref_axis',(-0.707106781186768,0.707106781186327,0.));
#11277=DIRECTION('center_axis',(-1.35644469630397E-12,-0.866025403784439,
-0.5));
#11278=DIRECTION('ref_axis',(7.83108736907191E-13,0.5,-0.866025403784439));
#11279=DIRECTION('',(0.,0.,-1.));
#11280=DIRECTION('center_axis',(1.,1.91935343509834E-12,0.));
#11281=DIRECTION('ref_axis',(1.91935343509834E-12,-1.,0.));
#11282=DIRECTION('center_axis',(1.,1.91935343509834E-12,0.));
#11283=DIRECTION('ref_axis',(0.,0.,1.));
#11284=DIRECTION('',(9.59676717549172E-13,-0.5,0.866025403784439));
#11285=DIRECTION('center_axis',(-1.62884833462111E-16,1.,0.));
#11286=DIRECTION('ref_axis',(1.,1.62884833462111E-16,0.));
#11287=DIRECTION('center_axis',(-1.62884833462111E-16,1.,0.));
#11288=DIRECTION('ref_axis',(0.,0.,-1.));
#11289=DIRECTION('',(0.5,8.14424167310554E-17,-0.866025403784439));
#11290=DIRECTION('center_axis',(-0.866025403784439,2.42308806056559E-16,
-0.5));
#11291=DIRECTION('ref_axis',(2.79794108807543E-16,1.,0.));
#11292=DIRECTION('center_axis',(-0.866025403784439,2.42308806056559E-16,
-0.5));
#11293=DIRECTION('ref_axis',(0.5,0.,-0.866025403784439));
#11294=DIRECTION('',(-2.79794108807543E-16,-1.,0.));
#11295=DIRECTION('center_axis',(-0.866025403784439,2.42308806056559E-16,
-0.5));
#11296=DIRECTION('ref_axis',(0.5,0.,-0.866025403784439));
#11297=DIRECTION('center_axis',(-1.,2.79168316070879E-12,0.));
#11298=DIRECTION('ref_axis',(2.79168316070879E-12,1.,0.));
#11299=DIRECTION('center_axis',(-1.,2.79168316070879E-12,0.));
#11300=DIRECTION('ref_axis',(0.,0.,-1.));
#11301=DIRECTION('',(1.3958415803544E-12,0.5,-0.866025403784439));
#11302=DIRECTION('center_axis',(-1.35644469630397E-12,-0.866025403784439,
-0.5));
#11303=DIRECTION('ref_axis',(-1.,1.56628742110387E-12,0.));
#11304=DIRECTION('center_axis',(-1.35644469630397E-12,-0.866025403784439,
-0.5));
#11305=DIRECTION('ref_axis',(0.,-0.5,0.866025403784439));
#11306=DIRECTION('',(1.,-1.56628742110387E-12,0.));
#11307=DIRECTION('center_axis',(0.,0.,-1.));
#11308=DIRECTION('ref_axis',(-1.,0.,0.));
#11309=DIRECTION('center_axis',(0.,0.,-1.));
#11310=DIRECTION('ref_axis',(-1.,0.,0.));
#11311=DIRECTION('center_axis',(0.,0.,-1.));
#11312=DIRECTION('ref_axis',(1.,0.,0.));
#11313=DIRECTION('center_axis',(-1.22464679914735E-16,-1.,0.));
#11314=DIRECTION('ref_axis',(1.,-1.22464679914735E-16,0.));
#11315=DIRECTION('center_axis',(0.,0.,1.));
#11316=DIRECTION('ref_axis',(1.,0.,0.));
#11317=DIRECTION('center_axis',(0.,0.,-1.));
#11318=DIRECTION('ref_axis',(-1.,0.,0.));
#11319=DIRECTION('center_axis',(0.,0.,-1.));
#11320=DIRECTION('ref_axis',(1.,0.,0.));
#11321=DIRECTION('center_axis',(0.,0.,-1.));
#11322=DIRECTION('ref_axis',(-1.,0.,0.));
#11323=DIRECTION('center_axis',(0.,0.,-1.));
#11324=DIRECTION('ref_axis',(1.,0.,0.));
#11325=DIRECTION('',(0.,0.,1.));
#11326=DIRECTION('center_axis',(0.,0.,-1.));
#11327=DIRECTION('ref_axis',(-1.,0.,0.));
#11328=DIRECTION('center_axis',(0.,0.,-1.));
#11329=DIRECTION('ref_axis',(-1.,0.,0.));
#11330=DIRECTION('',(-0.258819045102519,3.16961915143174E-17,0.965925826289069));
#11331=DIRECTION('center_axis',(0.,0.,-1.));
#11332=DIRECTION('ref_axis',(-1.,0.,0.));
#11333=DIRECTION('center_axis',(0.,0.,1.));
#11334=DIRECTION('ref_axis',(-1.,0.,0.));
#11335=DIRECTION('',(0.,0.,1.));
#11336=DIRECTION('center_axis',(0.,0.,-1.));
#11337=DIRECTION('ref_axis',(-1.,0.,0.));
#11338=DIRECTION('center_axis',(6.12323399573676E-17,0.,1.));
#11339=DIRECTION('ref_axis',(1.,0.,0.));
#11340=DIRECTION('center_axis',(1.22464679914735E-16,-1.,0.));
#11341=DIRECTION('ref_axis',(-1.,-1.22464679914735E-16,0.));
#11342=DIRECTION('center_axis',(0.,0.,-1.));
#11343=DIRECTION('ref_axis',(1.,0.,0.));
#11344=DIRECTION('center_axis',(0.,0.,-1.));
#11345=DIRECTION('ref_axis',(1.,0.,0.));
#11346=DIRECTION('center_axis',(0.,0.,-1.));
#11347=DIRECTION('ref_axis',(-1.,0.,0.));
#11348=DIRECTION('',(-0.087155742757872,1.06735001395738E-17,0.996194698090852));
#16259=CARTESIAN_POINT('',(0.,0.,0.));
#16260=CARTESIAN_POINT('Origin',(-0.744000000195138,0.744000000196221,1.2));
#16261=CARTESIAN_POINT('',(-0.744000000195138,0.248000000196221,1.15122809938326));
#16262=CARTESIAN_POINT('',(-0.248000000195138,0.744000000196666,1.15122809938313));
#16263=CARTESIAN_POINT('Ctrl Pts',(-0.744000000195138,0.248000000196221,
1.15122809938326));
#16264=CARTESIAN_POINT('Ctrl Pts',(-0.743548129195526,0.248000000196221,
1.15128162561029));
#16265=CARTESIAN_POINT('Ctrl Pts',(-0.743096462399636,0.248000617700407,
1.15133505381795));
#16266=CARTESIAN_POINT('Ctrl Pts',(-0.68084251616827,0.248170686680912,
1.1586889909138));
#16267=CARTESIAN_POINT('Ctrl Pts',(-0.614748859330863,0.260619583354249,
1.16502989619583));
#16268=CARTESIAN_POINT('Ctrl Pts',(-0.492966510303847,0.311166686726808,
1.17344391775669));
#16269=CARTESIAN_POINT('Ctrl Pts',(-0.437280006866291,0.349270066587974,
1.17551763482271));
#16270=CARTESIAN_POINT('Ctrl Pts',(-0.393275036726453,0.393275036727851,
1.17551763482269));
#16271=CARTESIAN_POINT('Ctrl Pts',(-0.349270066586615,0.437280006867729,
1.17551763482268));
#16272=CARTESIAN_POINT('Ctrl Pts',(-0.3111666867255,0.49296651030532,1.17344391775664));
#16273=CARTESIAN_POINT('Ctrl Pts',(-0.26061958335305,0.61474885933238,1.16502989619573));
#16274=CARTESIAN_POINT('Ctrl Pts',(-0.248170686679772,0.680842516169798,
1.15868899091368));
#16275=CARTESIAN_POINT('Ctrl Pts',(-0.248000617699323,0.743096462401038,
1.15133505381783));
#16276=CARTESIAN_POINT('Ctrl Pts',(-0.248000000195138,0.743548129196929,
1.15128162561017));
#16277=CARTESIAN_POINT('Ctrl Pts',(-0.248000000195138,0.744000000196666,
1.15122809938313));
#16278=CARTESIAN_POINT('',(-0.744000000195138,0.248000000196221,0.583389912843141));
#16279=CARTESIAN_POINT('',(-0.744000000195138,0.248000000196221,1.2));
#16280=CARTESIAN_POINT('',(-0.516876228118667,0.303056928861888,0.19));
#16281=CARTESIAN_POINT('Origin',(-0.744000000195138,0.744000000196221,0.583389912843142));
#16282=CARTESIAN_POINT('',(-0.303056928861701,0.51687622811801,0.19));
#16283=CARTESIAN_POINT('Origin',(-0.744000000195138,0.744000000196221,0.19));
#16284=CARTESIAN_POINT('',(-0.248000000195138,0.744000000196666,0.583389912846777));
#16285=CARTESIAN_POINT('Origin',(-0.744000000195138,0.744000000196221,0.583389912847341));
#16286=CARTESIAN_POINT('',(-0.248000000195138,0.744000000196666,1.2));
#16287=CARTESIAN_POINT('Origin',(-0.248000000194694,0.24800000019315,1.2));
#16288=CARTESIAN_POINT('',(-0.24800000019541,1.04682989872245,1.10790668314437));
#16289=CARTESIAN_POINT('Origin',(-0.248000000194471,-2.22346593631069E-13,
-5.12965591734105));
#16290=CARTESIAN_POINT('',(-0.248000000195362,0.993500000023809,1.01553658903582));
#16291=CARTESIAN_POINT('Origin',(-0.248000000195457,1.09999999999962,1.2));
#16292=CARTESIAN_POINT('',(0.248000000196041,1.04682989872314,1.10790668314423));
#16293=CARTESIAN_POINT('Origin',(2.9811416492917E-12,-1.91582141081592,
-4.02355591008723));
#16294=CARTESIAN_POINT('',(0.303056928861511,0.516876228118951,0.19));
#16295=CARTESIAN_POINT('',(-0.124000000097707,0.516876228118288,0.19));
#16296=CARTESIAN_POINT('',(0.248000000196085,0.744000000194883,0.583389912842355));
#16297=CARTESIAN_POINT('Origin',(0.744000000196085,0.744000000194955,0.583389912841147));
#16298=CARTESIAN_POINT('',(0.248000000196033,1.1000000000003,1.19999999999985));
#16299=CARTESIAN_POINT('Origin',(0.248000000196033,1.10000000000039,1.2));
#16300=CARTESIAN_POINT('',(0.248000000196085,0.744000000194883,1.1512280993833));
#16301=CARTESIAN_POINT('Origin',(0.248000000196193,3.61135222251268E-14,
-5.12965591734105));
#16302=CARTESIAN_POINT('',(0.248000000196085,0.744000000194883,1.2));
#16303=CARTESIAN_POINT('Origin',(0.744000000196085,0.744000000194955,1.2));
#16304=CARTESIAN_POINT('',(0.744000000196732,0.248000000194955,1.15122809938313));
#16305=CARTESIAN_POINT('Ctrl Pts',(0.248000000196085,0.744000000194883,
1.1512280993833));
#16306=CARTESIAN_POINT('Ctrl Pts',(0.248000000196085,0.743548129195249,
1.15128162561033));
#16307=CARTESIAN_POINT('Ctrl Pts',(0.24800061770027,0.743096462399337,1.15133505381799));
#16308=CARTESIAN_POINT('Ctrl Pts',(0.248170686680793,0.68084251616795,1.15868899091384));
#16309=CARTESIAN_POINT('Ctrl Pts',(0.260619583354148,0.614748859330546,
1.16502989619587));
#16310=CARTESIAN_POINT('Ctrl Pts',(0.311166686726741,0.492966510303544,
1.17344391775672));
#16311=CARTESIAN_POINT('Ctrl Pts',(0.349270066587923,0.437280006865998,
1.17551763482273));
#16312=CARTESIAN_POINT('Ctrl Pts',(0.393275036727812,0.393275036726173,
1.17551763482271));
#16313=CARTESIAN_POINT('Ctrl Pts',(0.437280006867702,0.349270066586347,
1.1755176348227));
#16314=CARTESIAN_POINT('Ctrl Pts',(0.492966510305304,0.311166686725247,
1.17344391775665));
#16315=CARTESIAN_POINT('Ctrl Pts',(0.614748859332378,0.26061958335283,1.16502989619575));
#16316=CARTESIAN_POINT('Ctrl Pts',(0.6808425161698,0.248170686679572,1.15868899091369));
#16317=CARTESIAN_POINT('Ctrl Pts',(0.743096462401062,0.24800061769914,1.15133505381783));
#16318=CARTESIAN_POINT('Ctrl Pts',(0.743548129196974,0.248000000194955,
1.15128162561017));
#16319=CARTESIAN_POINT('Ctrl Pts',(0.744000000196732,0.248000000194955,
1.15122809938313));
#16320=CARTESIAN_POINT('',(0.516876228118432,0.30305692886123,0.19));
#16321=CARTESIAN_POINT('Origin',(0.744000000196085,0.744000000194955,0.19));
#16322=CARTESIAN_POINT('',(0.744000000196732,0.248000000194955,0.583389912846289));
#16323=CARTESIAN_POINT('Origin',(0.744000000196085,0.744000000194955,0.583389912845349));
#16324=CARTESIAN_POINT('',(0.744000000196732,0.248000000194955,1.2));
#16325=CARTESIAN_POINT('Origin',(0.248000000196157,0.248000000194308,1.2));
#16326=CARTESIAN_POINT('',(1.04682989872277,0.24800000019535,1.10790668314432));
#16327=CARTESIAN_POINT('Origin',(-3.16340915708764E-13,0.248000000193984,
-5.12965591734105));
#16328=CARTESIAN_POINT('',(0.99350000002449,0.248000000195281,1.01553658903639));
#16329=CARTESIAN_POINT('Origin',(1.09999999999997,0.248000000195419,1.2));
#16330=CARTESIAN_POINT('',(1.04682989872287,-0.248000000195507,1.1079066831443));
#16331=CARTESIAN_POINT('Origin',(-1.91582141081591,-4.04170800382928E-13,
-4.02355591008723));
#16332=CARTESIAN_POINT('',(0.51687622811856,-0.3030569288607,0.19));
#16333=CARTESIAN_POINT('',(0.51687622811847,0.124000000097702,0.19));
#16334=CARTESIAN_POINT('',(0.744000000195517,-0.248000000195115,0.583389912844004));
#16335=CARTESIAN_POINT('Origin',(0.744000000194874,-0.744000000195115,0.583389912842708));
#16336=CARTESIAN_POINT('',(1.09999999999998,-0.248000000195576,1.19999999999984));
#16337=CARTESIAN_POINT('Origin',(1.10000000000007,-0.248000000195576,1.2));
#16338=CARTESIAN_POINT('',(0.744000000195517,-0.248000000195115,1.15122809938326));
#16339=CARTESIAN_POINT('Origin',(-3.14351440352569E-13,-0.24800000019415,
-5.12965591734105));
#16340=CARTESIAN_POINT('',(0.744000000195517,-0.248000000195115,1.2));
#16341=CARTESIAN_POINT('Origin',(-0.744000000195415,-0.744000000194864,
1.2));
#16342=CARTESIAN_POINT('',(-0.248000000195415,-0.744000000196249,1.15122809938316));
#16343=CARTESIAN_POINT('',(-0.744000000196312,-0.248000000194864,1.15122809938318));
#16344=CARTESIAN_POINT('Ctrl Pts',(-0.248000000195415,-0.744000000196249,
1.15122809938316));
#16345=CARTESIAN_POINT('Ctrl Pts',(-0.248000000195414,-0.74354812919633,
1.15128162561023));
#16346=CARTESIAN_POINT('Ctrl Pts',(-0.248000617699598,-0.743096462400134,
1.15133505381792));
#16347=CARTESIAN_POINT('Ctrl Pts',(-0.248170686680046,-0.680842516168463,
1.15868899091381));
#16348=CARTESIAN_POINT('Ctrl Pts',(-0.260619583353321,-0.614748859331044,
1.16502989619585));
#16349=CARTESIAN_POINT('Ctrl Pts',(-0.311166686725766,-0.49296651030398,
1.17344391775673));
#16350=CARTESIAN_POINT('Ctrl Pts',(-0.349270066586879,-0.437280006866388,
1.17551763482276));
#16351=CARTESIAN_POINT('Ctrl Pts',(-0.393275036726715,-0.393275036726509,
1.17551763482276));
#16352=CARTESIAN_POINT('Ctrl Pts',(-0.437280006866551,-0.349270066586629,
1.17551763482276));
#16353=CARTESIAN_POINT('Ctrl Pts',(-0.492966510304106,-0.311166686725461,
1.17344391775673));
#16354=CARTESIAN_POINT('Ctrl Pts',(-0.61474885933112,-0.260619583352896,
1.16502989619586));
#16355=CARTESIAN_POINT('Ctrl Pts',(-0.680842516168527,-0.248170686679557,
1.15868899091382));
#16356=CARTESIAN_POINT('Ctrl Pts',(-0.743096462400073,-0.248000617699049,
1.15133505381795));
#16357=CARTESIAN_POINT('Ctrl Pts',(-0.74354812919627,-0.248000000194863,
1.15128162561025));
#16358=CARTESIAN_POINT('Ctrl Pts',(-0.744000000196312,-0.248000000194864,
1.15122809938318));
#16359=CARTESIAN_POINT('',(-0.248000000195415,-0.744000000196249,0.58338991284606));
#16360=CARTESIAN_POINT('',(-0.248000000195415,-0.744000000196249,1.2));
#16361=CARTESIAN_POINT('',(-0.303056928861281,-0.516876228118006,0.19));
#16362=CARTESIAN_POINT('Origin',(-0.744000000195415,-0.744000000194864,
0.583389912845007));
#16363=CARTESIAN_POINT('',(-0.516876228118667,-0.303056928860673,0.19));
#16364=CARTESIAN_POINT('Origin',(-0.744000000195415,-0.744000000194864,
0.19));
#16365=CARTESIAN_POINT('',(-0.744000000196312,-0.248000000194864,0.583389912845176));
#16366=CARTESIAN_POINT('Origin',(-0.744000000195415,-0.744000000194864,
0.583389912843621));
#16367=CARTESIAN_POINT('',(-0.744000000196312,-0.248000000194864,1.2));
#16368=CARTESIAN_POINT('Origin',(-0.24800000019403,-0.248000000193966,1.2));
#16369=CARTESIAN_POINT('',(-1.04682989872298,-0.248000000195412,1.10790668314428));
#16370=CARTESIAN_POINT('Origin',(4.5589868649524E-13,-0.248000000193518,
-5.12965591734105));
#16371=CARTESIAN_POINT('',(-0.993500000024419,-0.248000000195315,1.01553658903588));
#16372=CARTESIAN_POINT('Origin',(0.744000000194874,-0.744000000195115,1.2));
#16373=CARTESIAN_POINT('',(0.248000000194874,-0.744000000196067,1.15122809938321));
#16374=CARTESIAN_POINT('Ctrl Pts',(0.744000000195517,-0.248000000195115,
1.15122809938326));
#16375=CARTESIAN_POINT('Ctrl Pts',(0.743548129195714,-0.248000000195114,
1.15128162561031));
#16376=CARTESIAN_POINT('Ctrl Pts',(0.743096462399633,-0.248000617699299,
1.15133505381799));
#16377=CARTESIAN_POINT('Ctrl Pts',(0.680842516168076,-0.248170686679796,
1.15868899091386));
#16378=CARTESIAN_POINT('Ctrl Pts',(0.614748859330666,-0.260619583353124,
1.1650298961959));
#16379=CARTESIAN_POINT('Ctrl Pts',(0.492966510303643,-0.311166686725667,
1.17344391775676));
#16380=CARTESIAN_POINT('Ctrl Pts',(0.437280006866081,-0.349270066586825,
1.17551763482279));
#16381=CARTESIAN_POINT('Ctrl Pts',(0.393275036726237,-0.393275036726696,
1.17551763482278));
#16382=CARTESIAN_POINT('Ctrl Pts',(0.349270066586393,-0.437280006866568,
1.17551763482278));
#16383=CARTESIAN_POINT('Ctrl Pts',(0.31116668672527,-0.492966510304154,
1.17344391775674));
#16384=CARTESIAN_POINT('Ctrl Pts',(0.260619583352803,-0.614748859331208,
1.16502989619586));
#16385=CARTESIAN_POINT('Ctrl Pts',(0.248170686679517,-0.680842516168625,
1.15868899091381));
#16386=CARTESIAN_POINT('Ctrl Pts',(0.248000617699059,-0.743096462400057,
1.15133505381795));
#16387=CARTESIAN_POINT('Ctrl Pts',(0.248000000194873,-0.743548129196139,
1.15128162561027));
#16388=CARTESIAN_POINT('Ctrl Pts',(0.248000000194874,-0.744000000196067,
1.15122809938321));
#16389=CARTESIAN_POINT('',(0.30305692886038,-0.516876228118955,0.19));
#16390=CARTESIAN_POINT('Origin',(0.744000000194874,-0.744000000195115,0.19));
#16391=CARTESIAN_POINT('',(0.248000000194874,-0.744000000196067,0.5833899128444));
#16392=CARTESIAN_POINT('Origin',(0.744000000194874,-0.744000000195115,0.583389912841405));
#16393=CARTESIAN_POINT('',(0.248000000194874,-0.744000000196067,1.2));
#16394=CARTESIAN_POINT('Origin',(0.248000000193922,-0.248000000194471,1.2));
#16395=CARTESIAN_POINT('',(0.248000000195456,-1.04682989872316,1.10790668314425));
#16396=CARTESIAN_POINT('Origin',(0.248000000193446,4.75999652275667E-13,
-5.12965591734105));
#16397=CARTESIAN_POINT('',(0.248000000195353,-0.993500000024651,1.01553658903593));
#16398=CARTESIAN_POINT('Origin',(-1.10000000000019,0.248000000196221,1.2));
#16399=CARTESIAN_POINT('',(-1.04682989872296,0.248000000196221,1.10790668314426));
#16400=CARTESIAN_POINT('Origin',(7.17605422133295E-15,0.248000000196221,
-5.12965591734105));
#16401=CARTESIAN_POINT('',(-1.10000000000019,0.248000000196221,1.2));
#16402=CARTESIAN_POINT('Origin',(-1.10000000000019,-0.248000000195508,1.2));
#16403=CARTESIAN_POINT('',(-1.04942373620595,-1.28517341949389E-16,1.11239934145138));
#16404=CARTESIAN_POINT('Origin',(1.91582141081578,-5.36035544273609E-16,
-4.02355591008731));
#16405=CARTESIAN_POINT('',(-0.516876228118667,-0.124000000097755,0.19));
#16406=CARTESIAN_POINT('Origin',(1.91582141081578,-5.36035544273609E-16,
-4.02355591008731));
#16407=CARTESIAN_POINT('Origin',(-0.248000000196409,-1.09999999999961,1.2));
#16408=CARTESIAN_POINT('',(-0.24800000019626,-1.04682989872243,1.10790668314434));
#16409=CARTESIAN_POINT('Origin',(-0.248000000193338,6.92337424395539E-13,
-5.12965591734105));
#16410=CARTESIAN_POINT('',(-0.248000000196409,-1.09999999999954,1.19999999999987));
#16411=CARTESIAN_POINT('Origin',(0.248000000195558,-1.10000000000039,1.2));
#16412=CARTESIAN_POINT('Origin',(3.00794342650252E-12,1.91582141081592,
-4.02355591008723));
#16413=CARTESIAN_POINT('',(0.124000000097801,-0.516876228118675,0.19));
#16414=CARTESIAN_POINT('Origin',(-5.91193760612896E-14,-1.66533453693773E-15,
0.19));
#16415=CARTESIAN_POINT('Origin',(0.,0.,-0.1));
#16416=CARTESIAN_POINT('',(0.939230484541328,-1.15022560655515E-16,0.));
#16417=CARTESIAN_POINT('Origin',(0.,0.,0.));
#16418=CARTESIAN_POINT('',(0.839230484541328,-1.02776092664042E-16,-0.1));
#16419=CARTESIAN_POINT('Origin',(0.939230484541328,-1.15022560655515E-16,
-0.1));
#16420=CARTESIAN_POINT('Origin',(0.,0.,-0.1));
#16421=CARTESIAN_POINT('Origin',(-0.839230484541328,0.,-7.24797437703358E-18));
#16422=CARTESIAN_POINT('',(2.15,-2.63299061816681E-16,0.));
#16423=CARTESIAN_POINT('Origin',(0.,0.,0.));
#16424=CARTESIAN_POINT('Origin',(0.,0.,-0.0749999999999998));
#16425=CARTESIAN_POINT('',(0.839230484541328,-1.02776092664042E-16,-0.15));
#16426=CARTESIAN_POINT('Origin',(0.,0.,-0.15));
#16427=CARTESIAN_POINT('',(0.839230484541328,-1.02776092664042E-16,-0.0749999999999998));
#16428=CARTESIAN_POINT('Origin',(0.,0.,-0.45));
#16429=CARTESIAN_POINT('',(0.96675,-1.1839272930757E-16,-0.625909310648334));
#16430=CARTESIAN_POINT('Origin',(0.,0.,-0.625909310648334));
#16431=CARTESIAN_POINT('',(0.919615242270664,-1.12620386289389E-16,-0.45));
#16432=CARTESIAN_POINT('Origin',(0.,0.,-3.375));
#16433=CARTESIAN_POINT('',(0.96675,1.1839272930757E-16,-6.));
#16434=CARTESIAN_POINT('Origin',(0.,0.,-6.));
#16435=CARTESIAN_POINT('',(0.96675,-1.1839272930757E-16,-3.375));
#16436=CARTESIAN_POINT('Origin',(0.,0.,-6.));
#16437=CARTESIAN_POINT('Origin',(7.21644966006352E-15,0.,-5.12965591734105));
#16438=CARTESIAN_POINT('',(-2.07563463599418,0.,0.85));
#16439=CARTESIAN_POINT('Origin',(7.21644966006352E-15,0.,-5.12965591734105));
#16440=CARTESIAN_POINT('',(2.07563463599418,-2.54191931316966E-16,0.85));
#16441=CARTESIAN_POINT('Origin',(0.,0.,0.85));
#16442=CARTESIAN_POINT('Origin',(0.,0.,0.85));
#16443=CARTESIAN_POINT('Origin',(0.,0.,0.425));
#16444=CARTESIAN_POINT('',(2.11281731799709,-2.58745496566823E-16,0.425));
#17024=UNCERTAINTY_MEASURE_WITH_UNIT(LENGTH_MEASURE(0.01),#17043,
'DISTANCE_ACCURACY_VALUE',
'Maximum model space distance between geometric entities at asserted c
onnectivities');
#17028=UNCERTAINTY_MEASURE_WITH_UNIT(LENGTH_MEASURE(0.01),#17043,
'DISTANCE_ACCURACY_VALUE',
'Maximum model space distance between geometric entities at asserted c
onnectivities');
#17038=(
GEOMETRIC_REPRESENTATION_CONTEXT(3)
GLOBAL_UNCERTAINTY_ASSIGNED_CONTEXT((#17024))
GLOBAL_UNIT_ASSIGNED_CONTEXT((#17043,#17045,#17046))
REPRESENTATION_CONTEXT('','3D')
);
#17042=(
GEOMETRIC_REPRESENTATION_CONTEXT(3)
GLOBAL_UNCERTAINTY_ASSIGNED_CONTEXT((#17028))
GLOBAL_UNIT_ASSIGNED_CONTEXT((#17043,#17045,#17046))
REPRESENTATION_CONTEXT('','3D')
);
#17043=(
LENGTH_UNIT()
NAMED_UNIT(*)
SI_UNIT(.MILLI.,.METRE.)
);
#17045=(
NAMED_UNIT(*)
PLANE_ANGLE_UNIT()
SI_UNIT($,.RADIAN.)
);
#17046=(
NAMED_UNIT(*)
SI_UNIT($,.STERADIAN.)
SOLID_ANGLE_UNIT()
);
#17056=SHAPE_DEFINITION_REPRESENTATION(#17069,#17094);
#17069=PRODUCT_DEFINITION_SHAPE('',$,#17108);
#17094=SHAPE_REPRESENTATION('',(#8995),#17038);
#17098=PRODUCT_DEFINITION_CONTEXT('part definition',#17139,'design');
#17108=PRODUCT_DEFINITION('BHS JIS B 1111 - M2x6 Steel 4.6 Plain',
'Binding Head Screw JIS B 1111 - M2x6 Steel 4.6 Plain v1',#17121,#17098);
#17121=PRODUCT_DEFINITION_FORMATION('',$,#17150);
#17139=APPLICATION_CONTEXT(
'Core Data for Automotive Mechanical Design Process');
#17140=PRODUCT_CONTEXT('part definition',#17139,'mechanical');
#17150=PRODUCT('BHS JIS B 1111 - M2x6 Steel 4.6 Plain',
'Binding Head Screw JIS B 1111 - M2x6 Steel 4.6 Plain v1',
'Binding Head Screw JIS B 1111 - M2x6',(#17140));
#17154=PRESENTATION_STYLE_ASSIGNMENT((#17155));
#17155=SURFACE_STYLE_USAGE(.BOTH.,#17156);
#17156=SURFACE_SIDE_STYLE('',(#17157));
#17157=SURFACE_STYLE_FILL_AREA(#17158);
#17158=FILL_AREA_STYLE('Steel - Satin',(#17159));
#17159=FILL_AREA_STYLE_COLOUR('Steel - Satin',#17160);
#17160=COLOUR_RGB('Steel - Satin', 0.09019608, 0.27058824, 0.51372549);
ENDSEC;
END-ISO-10303-21;
